ISO-10303-21;
HEADER;
/* Generated by software containing ST-Developer
 * from STEP Tools, Inc. (www.steptools.com) 
 */

FILE_DESCRIPTION(
/* description */ ('PAT-091'),
/* implementation_level */ '2;1');

FILE_NAME(
/* name */ 'Axle end keeper (4).step',
/* time_stamp */ '2026-10-27T15:34:44-07:00',
/* author */ (''),
/* organization */ (''),
/* preprocessor_version */ 'ST-DEVELOPER v20.2',
/* originating_system */ 'Autodesk Translation Framework v15.17.0.0',
/* authorisation */ '');

FILE_SCHEMA (('AUTOMOTIVE_DESIGN { 1 0 10303 214 3 1 1 }'));
ENDSEC;

DATA;
#10=MECHANICAL_DESIGN_GEOMETRIC_PRESENTATION_REPRESENTATION('',(#1007),#25100);
#787=SHAPE_REPRESENTATION_RELATIONSHIP('SRR','None',#25550,#897);
#897=ADVANCED_BREP_SHAPE_REPRESENTATION('',(#1129),#25020);
#1007=STYLED_ITEM('',(#26191),#1129);
#1129=MANIFOLD_SOLID_BREP('Body1',#13286);
#1420=FACE_BOUND('',#3401,.T.);
#1421=FACE_BOUND('',#3403,.T.);
#1811=PLANE('',#15221);
#1812=PLANE('',#15222);
#2375=FACE_OUTER_BOUND('',#3398,.T.);
#2376=FACE_OUTER_BOUND('',#3399,.T.);
#2377=FACE_OUTER_BOUND('',#3400,.T.);
#2378=FACE_OUTER_BOUND('',#3402,.T.);
#3398=EDGE_LOOP('',(#10272,#10273,#10274,#10275));
#3399=EDGE_LOOP('',(#10276,#10277,#10278,#10279));
#3400=EDGE_LOOP('',(#10280));
#3401=EDGE_LOOP('',(#10281));
#3402=EDGE_LOOP('',(#10282));
#3403=EDGE_LOOP('',(#10283));
#4495=LINE('',#22438,#5235);
#4496=LINE('',#22444,#5236);
#5235=VECTOR('',#18103,0.225000000000001);
#5236=VECTOR('',#18110,1.);
#5881=CIRCLE('',#15216,0.225000000000001);
#5882=CIRCLE('',#15217,0.225000000000001);
#5883=CIRCLE('',#15219,1.);
#5884=CIRCLE('',#15220,1.);
#6814=VERTEX_POINT('',#22435);
#6815=VERTEX_POINT('',#22437);
#6816=VERTEX_POINT('',#22441);
#6817=VERTEX_POINT('',#22443);
#8071=EDGE_CURVE('',#6814,#6814,#5881,.T.);
#8072=EDGE_CURVE('',#6814,#6815,#4495,.T.);
#8073=EDGE_CURVE('',#6815,#6815,#5882,.T.);
#8074=EDGE_CURVE('',#6816,#6816,#5883,.T.);
#8075=EDGE_CURVE('',#6816,#6817,#4496,.T.);
#8076=EDGE_CURVE('',#6817,#6817,#5884,.T.);
#10272=ORIENTED_EDGE('',*,*,#8071,.F.);
#10273=ORIENTED_EDGE('',*,*,#8072,.T.);
#10274=ORIENTED_EDGE('',*,*,#8073,.T.);
#10275=ORIENTED_EDGE('',*,*,#8072,.F.);
#10276=ORIENTED_EDGE('',*,*,#8074,.F.);
#10277=ORIENTED_EDGE('',*,*,#8075,.T.);
#10278=ORIENTED_EDGE('',*,*,#8076,.T.);
#10279=ORIENTED_EDGE('',*,*,#8075,.F.);
#10280=ORIENTED_EDGE('',*,*,#8074,.T.);
#10281=ORIENTED_EDGE('',*,*,#8071,.T.);
#10282=ORIENTED_EDGE('',*,*,#8076,.F.);
#10283=ORIENTED_EDGE('',*,*,#8073,.F.);
#12208=CYLINDRICAL_SURFACE('',#15215,0.225000000000001);
#12209=CYLINDRICAL_SURFACE('',#15218,1.);
#12742=ADVANCED_FACE('',(#2375),#12208,.F.);
#12743=ADVANCED_FACE('',(#2376),#12209,.T.);
#12744=ADVANCED_FACE('',(#2377,#1420),#1811,.T.);
#12745=ADVANCED_FACE('',(#2378,#1421),#1812,.F.);
#13286=CLOSED_SHELL('',(#12742,#12743,#12744,#12745));
#15214=AXIS2_PLACEMENT_3D('',#22433,#18097,#18098);
#15215=AXIS2_PLACEMENT_3D('',#22434,#18099,#18100);
#15216=AXIS2_PLACEMENT_3D('',#22436,#18101,#18102);
#15217=AXIS2_PLACEMENT_3D('',#22439,#18104,#18105);
#15218=AXIS2_PLACEMENT_3D('',#22440,#18106,#18107);
#15219=AXIS2_PLACEMENT_3D('',#22442,#18108,#18109);
#15220=AXIS2_PLACEMENT_3D('',#22445,#18111,#18112);
#15221=AXIS2_PLACEMENT_3D('',#22446,#18113,#18114);
#15222=AXIS2_PLACEMENT_3D('',#22447,#18115,#18116);
#18097=DIRECTION('axis',(0.,0.,1.));
#18098=DIRECTION('refdir',(1.,0.,0.));
#18099=DIRECTION('center_axis',(0.,1.,0.));
#18100=DIRECTION('ref_axis',(1.,0.,0.));
#18101=DIRECTION('center_axis',(0.,-1.,0.));
#18102=DIRECTION('ref_axis',(1.,0.,0.));
#18103=DIRECTION('',(0.,-1.,0.));
#18104=DIRECTION('center_axis',(0.,-1.,0.));
#18105=DIRECTION('ref_axis',(1.,0.,0.));
#18106=DIRECTION('center_axis',(0.,1.,0.));
#18107=DIRECTION('ref_axis',(1.,0.,0.));
#18108=DIRECTION('center_axis',(0.,1.,0.));
#18109=DIRECTION('ref_axis',(1.,0.,0.));
#18110=DIRECTION('',(0.,-1.,0.));
#18111=DIRECTION('center_axis',(0.,1.,0.));
#18112=DIRECTION('ref_axis',(1.,0.,0.));
#18113=DIRECTION('center_axis',(0.,1.,0.));
#18114=DIRECTION('ref_axis',(1.,0.,0.));
#18115=DIRECTION('center_axis',(0.,1.,0.));
#18116=DIRECTION('ref_axis',(1.,0.,0.));
#22433=CARTESIAN_POINT('',(0.,0.,0.));
#22434=CARTESIAN_POINT('Origin',(38.7298334620742,-6.2,3.));
#22435=CARTESIAN_POINT('',(38.5048334620742,-6.,3.));
#22436=CARTESIAN_POINT('Origin',(38.7298334620742,-6.,3.));
#22437=CARTESIAN_POINT('',(38.5048334620742,-6.2,3.));
#22438=CARTESIAN_POINT('',(38.5048334620742,-6.2,3.));
#22439=CARTESIAN_POINT('Origin',(38.7298334620742,-6.2,3.));
#22440=CARTESIAN_POINT('Origin',(38.7298334620742,-6.2,3.));
#22441=CARTESIAN_POINT('',(37.7298334620742,-6.,3.));
#22442=CARTESIAN_POINT('Origin',(38.7298334620742,-6.,3.));
#22443=CARTESIAN_POINT('',(37.7298334620742,-6.2,3.));
#22444=CARTESIAN_POINT('',(37.7298334620742,-6.2,3.));
#22445=CARTESIAN_POINT('Origin',(38.7298334620742,-6.2,3.));
#22446=CARTESIAN_POINT('Origin',(38.7298334620742,-6.,3.));
#22447=CARTESIAN_POINT('Origin',(38.7298334620742,-6.2,3.));
#24899=UNCERTAINTY_MEASURE_WITH_UNIT(LENGTH_MEASURE(0.001),#25101,
'DISTANCE_ACCURACY_VALUE',
'Maximum model space distance between geometric entities at asserted c
onnectivities');
#24979=UNCERTAINTY_MEASURE_WITH_UNIT(LENGTH_MEASURE(0.001),#25101,
'DISTANCE_ACCURACY_VALUE',
'Maximum model space distance between geometric entities at asserted c
onnectivities');
#25020=(
GEOMETRIC_REPRESENTATION_CONTEXT(3)
GLOBAL_UNCERTAINTY_ASSIGNED_CONTEXT((#24899))
GLOBAL_UNIT_ASSIGNED_CONTEXT((#25101,#25103,#25104))
REPRESENTATION_CONTEXT('','3D')
);
#25100=(
GEOMETRIC_REPRESENTATION_CONTEXT(3)
GLOBAL_UNCERTAINTY_ASSIGNED_CONTEXT((#24979))
GLOBAL_UNIT_ASSIGNED_CONTEXT((#25101,#25103,#25104))
REPRESENTATION_CONTEXT('','3D')
);
#25101=(
LENGTH_UNIT()
NAMED_UNIT(*)
SI_UNIT(.CENTI.,.METRE.)
);
#25103=(
NAMED_UNIT(*)
PLANE_ANGLE_UNIT()
SI_UNIT($,.RADIAN.)
);
#25104=(
NAMED_UNIT(*)
SI_UNIT($,.STERADIAN.)
SOLID_ANGLE_UNIT()
);
#25145=SHAPE_DEFINITION_REPRESENTATION(#25265,#25550);
#25265=PRODUCT_DEFINITION_SHAPE('',$,#25671);
#25550=SHAPE_REPRESENTATION('',(#15214),#25020);
#25630=PRODUCT_DEFINITION_CONTEXT('part definition',#25992,'design');
#25671=PRODUCT_DEFINITION('Axle end keeper (4)','Axle end keeper (4)',#25791,
#25630);
#25791=PRODUCT_DEFINITION_FORMATION('',$,#26034);
#25992=APPLICATION_CONTEXT(
'Core Data for Automotive Mechanical Design Process');
#25993=PRODUCT_CONTEXT('part definition',#25992,'mechanical');
#26034=PRODUCT('Axle end keeper (4)','Axle end keeper (4)',
'Axle end keeper (4)',(#25993));
#26185=COLOUR_RGB('Grey',0.48,0.52,0.57);
#26186=FILL_AREA_STYLE_COLOUR('',#26185);
#26187=FILL_AREA_STYLE('',(#26186));
#26188=SURFACE_STYLE_FILL_AREA(#26187);
#26189=SURFACE_SIDE_STYLE('',(#26188));
#26190=SURFACE_STYLE_USAGE(.BOTH.,#26189);
#26191=PRESENTATION_STYLE_ASSIGNMENT((#26190));
ENDSEC;
END-ISO-10303-21;
